ISO-10303-21;
HEADER;
/* Generated by software containing ST-Developer
 * from STEP Tools, Inc. (www.steptools.com) 
 */

FILE_DESCRIPTION(
/* description */ ('Bearing-mounted hook block'),
/* implementation_level */ '2;1');

FILE_NAME(
/* name */ 'Flat Washer - M8.step',
/* time_stamp */ '2026-10-28T22:30:11-07:00',
/* author */ (''),
/* organization */ (''),
/* preprocessor_version */ 'ST-DEVELOPER v20.2',
/* originating_system */ 'Autodesk Translation Framework v15.17.0.0',
/* authorisation */ '');

FILE_SCHEMA (('AUTOMOTIVE_DESIGN { 1 0 10303 214 3 1 1 }'));
ENDSEC;

DATA;
#10=MECHANICAL_DESIGN_GEOMETRIC_PRESENTATION_REPRESENTATION('',(#332),#7609);
#284=SHAPE_REPRESENTATION_RELATIONSHIP('SRR','None',#7731,#308);
#308=ADVANCED_BREP_SHAPE_REPRESENTATION('',(#363),#7591);
#332=STYLED_ITEM('',(#7938),#363);
#363=MANIFOLD_SOLID_BREP('Body1',#3929);
#477=LINE('',#6437,#707);
#478=LINE('',#6443,#708);
#707=VECTOR('',#5186,0.42);
#708=VECTOR('',#5193,0.8);
#876=CYLINDRICAL_SURFACE('',#4385,0.42);
#877=CYLINDRICAL_SURFACE('',#4388,0.8);
#955=FACE_BOUND('',#1353,.T.);
#956=FACE_BOUND('',#1355,.T.);
#1080=FACE_OUTER_BOUND('',#1350,.T.);
#1081=FACE_OUTER_BOUND('',#1351,.T.);
#1082=FACE_OUTER_BOUND('',#1352,.T.);
#1083=FACE_OUTER_BOUND('',#1354,.T.);
#1350=EDGE_LOOP('',(#2926,#2927,#2928,#2929));
#1351=EDGE_LOOP('',(#2930,#2931,#2932,#2933));
#1352=EDGE_LOOP('',(#2934));
#1353=EDGE_LOOP('',(#2935));
#1354=EDGE_LOOP('',(#2936));
#1355=EDGE_LOOP('',(#2937));
#1628=CIRCLE('',#4386,0.42);
#1629=CIRCLE('',#4387,0.42);
#1630=CIRCLE('',#4389,0.8);
#1631=CIRCLE('',#4390,0.8);
#1889=VERTEX_POINT('',#6434);
#1890=VERTEX_POINT('',#6436);
#1891=VERTEX_POINT('',#6440);
#1892=VERTEX_POINT('',#6442);
#2273=EDGE_CURVE('',#1889,#1889,#1628,.T.);
#2274=EDGE_CURVE('',#1889,#1890,#477,.T.);
#2275=EDGE_CURVE('',#1890,#1890,#1629,.T.);
#2276=EDGE_CURVE('',#1891,#1891,#1630,.T.);
#2277=EDGE_CURVE('',#1891,#1892,#478,.T.);
#2278=EDGE_CURVE('',#1892,#1892,#1631,.T.);
#2926=ORIENTED_EDGE('',*,*,#2273,.F.);
#2927=ORIENTED_EDGE('',*,*,#2274,.T.);
#2928=ORIENTED_EDGE('',*,*,#2275,.T.);
#2929=ORIENTED_EDGE('',*,*,#2274,.F.);
#2930=ORIENTED_EDGE('',*,*,#2276,.F.);
#2931=ORIENTED_EDGE('',*,*,#2277,.T.);
#2932=ORIENTED_EDGE('',*,*,#2278,.T.);
#2933=ORIENTED_EDGE('',*,*,#2277,.F.);
#2934=ORIENTED_EDGE('',*,*,#2276,.T.);
#2935=ORIENTED_EDGE('',*,*,#2273,.T.);
#2936=ORIENTED_EDGE('',*,*,#2278,.F.);
#2937=ORIENTED_EDGE('',*,*,#2275,.F.);
#3604=PLANE('',#4391);
#3605=PLANE('',#4392);
#3762=ADVANCED_FACE('',(#1080),#876,.F.);
#3763=ADVANCED_FACE('',(#1081),#877,.T.);
#3764=ADVANCED_FACE('',(#1082,#955),#3604,.T.);
#3765=ADVANCED_FACE('',(#1083,#956),#3605,.F.);
#3929=CLOSED_SHELL('',(#3762,#3763,#3764,#3765));
#4384=AXIS2_PLACEMENT_3D('',#6432,#5180,#5181);
#4385=AXIS2_PLACEMENT_3D('',#6433,#5182,#5183);
#4386=AXIS2_PLACEMENT_3D('',#6435,#5184,#5185);
#4387=AXIS2_PLACEMENT_3D('',#6438,#5187,#5188);
#4388=AXIS2_PLACEMENT_3D('',#6439,#5189,#5190);
#4389=AXIS2_PLACEMENT_3D('',#6441,#5191,#5192);
#4390=AXIS2_PLACEMENT_3D('',#6444,#5194,#5195);
#4391=AXIS2_PLACEMENT_3D('',#6445,#5196,#5197);
#4392=AXIS2_PLACEMENT_3D('',#6446,#5198,#5199);
#5180=DIRECTION('axis',(0.,0.,1.));
#5181=DIRECTION('refdir',(1.,0.,0.));
#5182=DIRECTION('center_axis',(0.,1.,0.));
#5183=DIRECTION('ref_axis',(1.,0.,0.));
#5184=DIRECTION('center_axis',(0.,-1.,0.));
#5185=DIRECTION('ref_axis',(1.,0.,0.));
#5186=DIRECTION('',(0.,-1.,0.));
#5187=DIRECTION('center_axis',(0.,-1.,0.));
#5188=DIRECTION('ref_axis',(1.,0.,0.));
#5189=DIRECTION('center_axis',(0.,1.,0.));
#5190=DIRECTION('ref_axis',(1.,0.,0.));
#5191=DIRECTION('center_axis',(0.,1.,0.));
#5192=DIRECTION('ref_axis',(1.,0.,0.));
#5193=DIRECTION('',(0.,-1.,0.));
#5194=DIRECTION('center_axis',(0.,1.,0.));
#5195=DIRECTION('ref_axis',(1.,0.,0.));
#5196=DIRECTION('center_axis',(0.,1.,0.));
#5197=DIRECTION('ref_axis',(1.,0.,0.));
#5198=DIRECTION('center_axis',(0.,1.,0.));
#5199=DIRECTION('ref_axis',(1.,0.,0.));
#6432=CARTESIAN_POINT('',(0.,0.,0.));
#6433=CARTESIAN_POINT('Origin',(0.,0.,0.));
#6434=CARTESIAN_POINT('',(-0.42,0.16,5.14351655641888E-17));
#6435=CARTESIAN_POINT('Origin',(0.,0.16,0.));
#6436=CARTESIAN_POINT('',(-0.42,0.,5.14351655641888E-17));
#6437=CARTESIAN_POINT('',(-0.42,0.,5.14351655641888E-17));
#6438=CARTESIAN_POINT('Origin',(0.,0.,0.));
#6439=CARTESIAN_POINT('Origin',(0.,0.,0.));
#6440=CARTESIAN_POINT('',(-0.8,0.16,9.79717439317883E-17));
#6441=CARTESIAN_POINT('Origin',(0.,0.16,0.));
#6442=CARTESIAN_POINT('',(-0.8,0.,9.79717439317883E-17));
#6443=CARTESIAN_POINT('',(-0.8,0.,9.79717439317883E-17));
#6444=CARTESIAN_POINT('Origin',(0.,0.,0.));
#6445=CARTESIAN_POINT('Origin',(0.,0.16,0.));
#6446=CARTESIAN_POINT('Origin',(0.,0.,0.));
#7561=UNCERTAINTY_MEASURE_WITH_UNIT(LENGTH_MEASURE(0.001),#7610,
'DISTANCE_ACCURACY_VALUE',
'Maximum model space distance between geometric entities at asserted c
onnectivities');
#7579=UNCERTAINTY_MEASURE_WITH_UNIT(LENGTH_MEASURE(0.001),#7610,
'DISTANCE_ACCURACY_VALUE',
'Maximum model space distance between geometric entities at asserted c
onnectivities');
#7591=(
GEOMETRIC_REPRESENTATION_CONTEXT(3)
GLOBAL_UNCERTAINTY_ASSIGNED_CONTEXT((#7561))
GLOBAL_UNIT_ASSIGNED_CONTEXT((#7610,#7612,#7613))
REPRESENTATION_CONTEXT('','3D')
);
#7609=(
GEOMETRIC_REPRESENTATION_CONTEXT(3)
GLOBAL_UNCERTAINTY_ASSIGNED_CONTEXT((#7579))
GLOBAL_UNIT_ASSIGNED_CONTEXT((#7610,#7612,#7613))
REPRESENTATION_CONTEXT('','3D')
);
#7610=(
LENGTH_UNIT()
NAMED_UNIT(*)
SI_UNIT(.CENTI.,.METRE.)
);
#7612=(
NAMED_UNIT(*)
PLANE_ANGLE_UNIT()
SI_UNIT($,.RADIAN.)
);
#7613=(
NAMED_UNIT(*)
SI_UNIT($,.STERADIAN.)
SOLID_ANGLE_UNIT()
);
#7625=SHAPE_DEFINITION_REPRESENTATION(#7654,#7731);
#7654=PRODUCT_DEFINITION_SHAPE('',$,#7761);
#7731=SHAPE_REPRESENTATION('',(#4384),#7591);
#7749=PRODUCT_DEFINITION_CONTEXT('part definition',#7838,'design');
#7761=PRODUCT_DEFINITION('Flat Washer - M8','Flat Washer - M8',#7790,#7749);
#7790=PRODUCT_DEFINITION_FORMATION('',$,#7851);
#7838=APPLICATION_CONTEXT(
'Core Data for Automotive Mechanical Design Process');
#7839=PRODUCT_CONTEXT('part definition',#7838,'mechanical');
#7851=PRODUCT('Flat Washer - M8','Flat Washer - M8','Flat Washer - M8',
(#7839));
#7932=COLOUR_RGB('Black',0.12,0.14,0.17);
#7933=FILL_AREA_STYLE_COLOUR('',#7932);
#7934=FILL_AREA_STYLE('',(#7933));
#7935=SURFACE_STYLE_FILL_AREA(#7934);
#7936=SURFACE_SIDE_STYLE('',(#7935));
#7937=SURFACE_STYLE_USAGE(.BOTH.,#7936);
#7938=PRESENTATION_STYLE_ASSIGNMENT((#7937));
ENDSEC;
END-ISO-10303-21;
